ISO-10303-21;
HEADER;
/* Generated by software containing ST-Developer
 * from STEP Tools, Inc. (www.steptools.com) 
 */

FILE_DESCRIPTION(
/* description */ ('', 'CAx-IF Rec.Pracs.---Representation and Presentation of Product Manufa
cturing Information (PMI)---4.0---2014-10-13'),
/* implementation_level */ '2;1');

FILE_NAME(
/* name */ 'Bearing Housing Socket Screws.step',
/* time_stamp */ '2026-10-28T23:00:48+01:00',
/* author */ (''),
/* organization */ (''),
/* preprocessor_version */ 'ST-DEVELOPER v20.2',
/* originating_system */ 'Autodesk Translation Framework v15.17.0.0',
/* authorisation */ '');

FILE_SCHEMA (('AP242_MANAGED_MODEL_BASED_3D_ENGINEERING_MIM_LF { 1 0 10303 442 2 1 4 }'));
ENDSEC;

DATA;
#10=MECHANICAL_DESIGN_GEOMETRIC_PRESENTATION_REPRESENTATION('',(#963),#61811);
#476=(
BOUNDED_CURVE()
B_SPLINE_CURVE(2,(#51009,#51010,#51011),.UNSPECIFIED.,.F.,.F.)
B_SPLINE_CURVE_WITH_KNOTS((3,3),(0.,0.58421806903896),.UNSPECIFIED.)
CURVE()
GEOMETRIC_REPRESENTATION_ITEM()
RATIONAL_B_SPLINE_CURVE((1.,1.15470053837925,1.))
REPRESENTATION_ITEM('')
);
#477=(
BOUNDED_CURVE()
B_SPLINE_CURVE(2,(#51016,#51017,#51018),.UNSPECIFIED.,.F.,.F.)
B_SPLINE_CURVE_WITH_KNOTS((3,3),(0.,0.584218069038959),.UNSPECIFIED.)
CURVE()
GEOMETRIC_REPRESENTATION_ITEM()
RATIONAL_B_SPLINE_CURVE((1.,1.15470053837925,1.))
REPRESENTATION_ITEM('')
);
#478=(
BOUNDED_CURVE()
B_SPLINE_CURVE(2,(#51022,#51023,#51024),.UNSPECIFIED.,.F.,.F.)
B_SPLINE_CURVE_WITH_KNOTS((3,3),(0.,0.584218069038959),.UNSPECIFIED.)
CURVE()
GEOMETRIC_REPRESENTATION_ITEM()
RATIONAL_B_SPLINE_CURVE((1.,1.15470053837925,1.))
REPRESENTATION_ITEM('')
);
#479=(
BOUNDED_CURVE()
B_SPLINE_CURVE(2,(#51028,#51029,#51030),.UNSPECIFIED.,.F.,.F.)
B_SPLINE_CURVE_WITH_KNOTS((3,3),(0.,0.58421806903896),.UNSPECIFIED.)
CURVE()
GEOMETRIC_REPRESENTATION_ITEM()
RATIONAL_B_SPLINE_CURVE((1.,1.15470053837925,1.))
REPRESENTATION_ITEM('')
);
#480=(
BOUNDED_CURVE()
B_SPLINE_CURVE(2,(#51034,#51035,#51036),.UNSPECIFIED.,.F.,.F.)
B_SPLINE_CURVE_WITH_KNOTS((3,3),(0.,0.292109034519478),.UNSPECIFIED.)
CURVE()
GEOMETRIC_REPRESENTATION_ITEM()
RATIONAL_B_SPLINE_CURVE((1.,1.07735026918962,1.07735026918962))
REPRESENTATION_ITEM('')
);
#481=(
BOUNDED_CURVE()
B_SPLINE_CURVE(2,(#51039,#51040,#51041),.UNSPECIFIED.,.F.,.F.)
B_SPLINE_CURVE_WITH_KNOTS((3,3),(0.292109034519478,0.584218069038959),
 .UNSPECIFIED.)
CURVE()
GEOMETRIC_REPRESENTATION_ITEM()
RATIONAL_B_SPLINE_CURVE((1.07735026918962,1.07735026918963,1.))
REPRESENTATION_ITEM('')
);
#482=(
BOUNDED_CURVE()
B_SPLINE_CURVE(2,(#51043,#51044,#51045),.UNSPECIFIED.,.F.,.F.)
B_SPLINE_CURVE_WITH_KNOTS((3,3),(0.,0.584218069038959),.UNSPECIFIED.)
CURVE()
GEOMETRIC_REPRESENTATION_ITEM()
RATIONAL_B_SPLINE_CURVE((1.,1.15470053837925,1.))
REPRESENTATION_ITEM('')
);
#565=CONICAL_SURFACE('',#34403,5.46323125,0.785398163397447);
#566=CONICAL_SURFACE('',#34419,2.88675134594813,1.0471975511966);
#888=TOROIDAL_SURFACE('',#34393,6.1,0.1);
#889=TOROIDAL_SURFACE('',#34406,7.8,1.2);
#913=SHAPE_REPRESENTATION_RELATIONSHIP('SRR','None',#61971,#938);
#938=ADVANCED_BREP_SHAPE_REPRESENTATION('',(#1002),#61784);
#963=STYLED_ITEM('',(#62163),#1002);
#1002=MANIFOLD_SOLID_BREP('Body1',#33793);
#1093=CYLINDRICAL_SURFACE('',#34398,6.);
#1094=CYLINDRICAL_SURFACE('',#34412,9.);
#1897=FACE_BOUND('',#6272,.T.);
#1898=FACE_BOUND('',#6277,.T.);
#2385=CIRCLE('',#34394,6.);
#2386=CIRCLE('',#34395,6.);
#2387=CIRCLE('',#34396,0.1);
#2388=CIRCLE('',#34397,6.1);
#2389=CIRCLE('',#34399,6.);
#2390=CIRCLE('',#34400,6.);
#2391=CIRCLE('',#34402,9.);
#2392=CIRCLE('',#34404,4.9264625);
#2393=CIRCLE('',#34407,9.);
#2394=CIRCLE('',#34408,9.);
#2395=CIRCLE('',#34409,1.2);
#2396=CIRCLE('',#34410,7.8);
#4372=FACE_OUTER_BOUND('',#6269,.T.);
#4373=FACE_OUTER_BOUND('',#6270,.T.);
#4374=FACE_OUTER_BOUND('',#6271,.T.);
#4375=FACE_OUTER_BOUND('',#6273,.T.);
#4376=FACE_OUTER_BOUND('',#6274,.T.);
#4377=FACE_OUTER_BOUND('',#6275,.T.);
#4378=FACE_OUTER_BOUND('',#6276,.T.);
#4379=FACE_OUTER_BOUND('',#6278,.T.);
#4380=FACE_OUTER_BOUND('',#6279,.T.);
#4381=FACE_OUTER_BOUND('',#6280,.T.);
#4382=FACE_OUTER_BOUND('',#6281,.T.);
#4383=FACE_OUTER_BOUND('',#6282,.T.);
#4384=FACE_OUTER_BOUND('',#6283,.T.);
#4385=FACE_OUTER_BOUND('',#6284,.T.);
#4386=FACE_OUTER_BOUND('',#6285,.T.);
#6269=EDGE_LOOP('',(#22088,#22089,#22090,#22091,#22092));
#6270=EDGE_LOOP('',(#22093,#22094,#22095,#22096,#22097,#22098));
#6271=EDGE_LOOP('',(#22099));
#6272=EDGE_LOOP('',(#22100));
#6273=EDGE_LOOP('',(#22101,#22102,#22103,#22104,#22105));
#6274=EDGE_LOOP('',(#22106));
#6275=EDGE_LOOP('',(#22107,#22108,#22109,#22110,#22111));
#6276=EDGE_LOOP('',(#22112));
#6277=EDGE_LOOP('',(#22113,#22114,#22115,#22116,#22117,#22118));
#6278=EDGE_LOOP('',(#22119,#22120,#22121,#22122,#22123));
#6279=EDGE_LOOP('',(#22124,#22125,#22126,#22127));
#6280=EDGE_LOOP('',(#22128,#22129,#22130,#22131));
#6281=EDGE_LOOP('',(#22132,#22133,#22134,#22135));
#6282=EDGE_LOOP('',(#22136,#22137,#22138,#22139));
#6283=EDGE_LOOP('',(#22140,#22141,#22142,#22143,#22144));
#6284=EDGE_LOOP('',(#22145,#22146,#22147,#22148));
#6285=EDGE_LOOP('',(#22149,#22150,#22151,#22152,#22153,#22154,#22155,#22156,
#22157));
#8477=LINE('',#50974,#11024);
#8478=LINE('',#50980,#11025);
#8479=LINE('',#50994,#11026);
#8480=LINE('',#50996,#11027);
#8481=LINE('',#50998,#11028);
#8482=LINE('',#51000,#11029);
#8483=LINE('',#51002,#11030);
#8484=LINE('',#51003,#11031);
#8485=LINE('',#51005,#11032);
#8486=LINE('',#51012,#11033);
#8487=LINE('',#51013,#11034);
#8488=LINE('',#51019,#11035);
#8489=LINE('',#51025,#11036);
#8490=LINE('',#51031,#11037);
#8491=LINE('',#51038,#11038);
#8492=LINE('',#51048,#11039);
#11024=VECTOR('',#38875,6.);
#11025=VECTOR('',#38882,5.46323125);
#11026=VECTOR('',#38899,10.);
#11027=VECTOR('',#38900,10.);
#11028=VECTOR('',#38901,10.);
#11029=VECTOR('',#38902,10.);
#11030=VECTOR('',#38903,10.);
#11031=VECTOR('',#38904,10.);
#11032=VECTOR('',#38907,9.);
#11033=VECTOR('',#38910,10.);
#11034=VECTOR('',#38911,10.);
#11035=VECTOR('',#38914,10.);
#11036=VECTOR('',#38917,10.);
#11037=VECTOR('',#38920,10.);
#11038=VECTOR('',#38923,10.);
#11039=VECTOR('',#38928,2.88675134594813);
#13626=VERTEX_POINT('',#50962);
#13627=VERTEX_POINT('',#50963);
#13628=VERTEX_POINT('',#50966);
#13629=VERTEX_POINT('',#50970);
#13630=VERTEX_POINT('',#50971);
#13631=VERTEX_POINT('',#50976);
#13632=VERTEX_POINT('',#50979);
#13633=VERTEX_POINT('',#50984);
#13634=VERTEX_POINT('',#50985);
#13635=VERTEX_POINT('',#50988);
#13636=VERTEX_POINT('',#50992);
#13637=VERTEX_POINT('',#50993);
#13638=VERTEX_POINT('',#50995);
#13639=VERTEX_POINT('',#50997);
#13640=VERTEX_POINT('',#50999);
#13641=VERTEX_POINT('',#51001);
#13642=VERTEX_POINT('',#51007);
#13643=VERTEX_POINT('',#51008);
#13644=VERTEX_POINT('',#51015);
#13645=VERTEX_POINT('',#51021);
#13646=VERTEX_POINT('',#51027);
#13647=VERTEX_POINT('',#51033);
#13648=VERTEX_POINT('',#51037);
#13649=VERTEX_POINT('',#51047);
#16946=EDGE_CURVE('',#13626,#13627,#2385,.T.);
#16947=EDGE_CURVE('',#13627,#13626,#2386,.T.);
#16948=EDGE_CURVE('',#13626,#13628,#2387,.T.);
#16949=EDGE_CURVE('',#13628,#13628,#2388,.T.);
#16950=EDGE_CURVE('',#13629,#13630,#2389,.T.);
#16951=EDGE_CURVE('',#13630,#13629,#2390,.T.);
#16952=EDGE_CURVE('',#13630,#13627,#8477,.T.);
#16953=EDGE_CURVE('',#13631,#13631,#2391,.T.);
#16954=EDGE_CURVE('',#13629,#13632,#8478,.T.);
#16955=EDGE_CURVE('',#13632,#13632,#2392,.T.);
#16956=EDGE_CURVE('',#13633,#13634,#2393,.T.);
#16957=EDGE_CURVE('',#13634,#13633,#2394,.T.);
#16958=EDGE_CURVE('',#13633,#13635,#2395,.T.);
#16959=EDGE_CURVE('',#13635,#13635,#2396,.T.);
#16960=EDGE_CURVE('',#13636,#13637,#8479,.T.);
#16961=EDGE_CURVE('',#13637,#13638,#8480,.T.);
#16962=EDGE_CURVE('',#13638,#13639,#8481,.T.);
#16963=EDGE_CURVE('',#13639,#13640,#8482,.T.);
#16964=EDGE_CURVE('',#13640,#13641,#8483,.T.);
#16965=EDGE_CURVE('',#13641,#13636,#8484,.T.);
#16966=EDGE_CURVE('',#13631,#13634,#8485,.T.);
#16967=EDGE_CURVE('',#13642,#13643,#476,.T.);
#16968=EDGE_CURVE('',#13642,#13641,#8486,.T.);
#16969=EDGE_CURVE('',#13643,#13640,#8487,.T.);
#16970=EDGE_CURVE('',#13644,#13642,#477,.T.);
#16971=EDGE_CURVE('',#13644,#13636,#8488,.T.);
#16972=EDGE_CURVE('',#13645,#13644,#478,.T.);
#16973=EDGE_CURVE('',#13645,#13637,#8489,.T.);
#16974=EDGE_CURVE('',#13646,#13645,#479,.T.);
#16975=EDGE_CURVE('',#13638,#13646,#8490,.T.);
#16976=EDGE_CURVE('',#13643,#13647,#480,.T.);
#16977=EDGE_CURVE('',#13648,#13639,#8491,.T.);
#16978=EDGE_CURVE('',#13647,#13648,#481,.T.);
#16979=EDGE_CURVE('',#13648,#13646,#482,.T.);
#16980=EDGE_CURVE('',#13649,#13647,#8492,.T.);
#22088=ORIENTED_EDGE('',*,*,#16946,.T.);
#22089=ORIENTED_EDGE('',*,*,#16947,.T.);
#22090=ORIENTED_EDGE('',*,*,#16948,.T.);
#22091=ORIENTED_EDGE('',*,*,#16949,.T.);
#22092=ORIENTED_EDGE('',*,*,#16948,.F.);
#22093=ORIENTED_EDGE('',*,*,#16950,.F.);
#22094=ORIENTED_EDGE('',*,*,#16951,.F.);
#22095=ORIENTED_EDGE('',*,*,#16952,.T.);
#22096=ORIENTED_EDGE('',*,*,#16946,.F.);
#22097=ORIENTED_EDGE('',*,*,#16947,.F.);
#22098=ORIENTED_EDGE('',*,*,#16952,.F.);
#22099=ORIENTED_EDGE('',*,*,#16953,.T.);
#22100=ORIENTED_EDGE('',*,*,#16949,.F.);
#22101=ORIENTED_EDGE('',*,*,#16950,.T.);
#22102=ORIENTED_EDGE('',*,*,#16951,.T.);
#22103=ORIENTED_EDGE('',*,*,#16954,.T.);
#22104=ORIENTED_EDGE('',*,*,#16955,.T.);
#22105=ORIENTED_EDGE('',*,*,#16954,.F.);
#22106=ORIENTED_EDGE('',*,*,#16955,.F.);
#22107=ORIENTED_EDGE('',*,*,#16956,.T.);
#22108=ORIENTED_EDGE('',*,*,#16957,.T.);
#22109=ORIENTED_EDGE('',*,*,#16958,.T.);
#22110=ORIENTED_EDGE('',*,*,#16959,.T.);
#22111=ORIENTED_EDGE('',*,*,#16958,.F.);
#22112=ORIENTED_EDGE('',*,*,#16959,.F.);
#22113=ORIENTED_EDGE('',*,*,#16960,.T.);
#22114=ORIENTED_EDGE('',*,*,#16961,.T.);
#22115=ORIENTED_EDGE('',*,*,#16962,.T.);
#22116=ORIENTED_EDGE('',*,*,#16963,.T.);
#22117=ORIENTED_EDGE('',*,*,#16964,.T.);
#22118=ORIENTED_EDGE('',*,*,#16965,.T.);
#22119=ORIENTED_EDGE('',*,*,#16953,.F.);
#22120=ORIENTED_EDGE('',*,*,#16966,.T.);
#22121=ORIENTED_EDGE('',*,*,#16956,.F.);
#22122=ORIENTED_EDGE('',*,*,#16957,.F.);
#22123=ORIENTED_EDGE('',*,*,#16966,.F.);
#22124=ORIENTED_EDGE('',*,*,#16967,.F.);
#22125=ORIENTED_EDGE('',*,*,#16968,.T.);
#22126=ORIENTED_EDGE('',*,*,#16964,.F.);
#22127=ORIENTED_EDGE('',*,*,#16969,.F.);
#22128=ORIENTED_EDGE('',*,*,#16970,.F.);
#22129=ORIENTED_EDGE('',*,*,#16971,.T.);
#22130=ORIENTED_EDGE('',*,*,#16965,.F.);
#22131=ORIENTED_EDGE('',*,*,#16968,.F.);
#22132=ORIENTED_EDGE('',*,*,#16972,.F.);
#22133=ORIENTED_EDGE('',*,*,#16973,.T.);
#22134=ORIENTED_EDGE('',*,*,#16960,.F.);
#22135=ORIENTED_EDGE('',*,*,#16971,.F.);
#22136=ORIENTED_EDGE('',*,*,#16974,.F.);
#22137=ORIENTED_EDGE('',*,*,#16975,.F.);
#22138=ORIENTED_EDGE('',*,*,#16961,.F.);
#22139=ORIENTED_EDGE('',*,*,#16973,.F.);
#22140=ORIENTED_EDGE('',*,*,#16976,.F.);
#22141=ORIENTED_EDGE('',*,*,#16969,.T.);
#22142=ORIENTED_EDGE('',*,*,#16963,.F.);
#22143=ORIENTED_EDGE('',*,*,#16977,.F.);
#22144=ORIENTED_EDGE('',*,*,#16978,.F.);
#22145=ORIENTED_EDGE('',*,*,#16979,.F.);
#22146=ORIENTED_EDGE('',*,*,#16977,.T.);
#22147=ORIENTED_EDGE('',*,*,#16962,.F.);
#22148=ORIENTED_EDGE('',*,*,#16975,.T.);
#22149=ORIENTED_EDGE('',*,*,#16980,.T.);
#22150=ORIENTED_EDGE('',*,*,#16978,.T.);
#22151=ORIENTED_EDGE('',*,*,#16979,.T.);
#22152=ORIENTED_EDGE('',*,*,#16974,.T.);
#22153=ORIENTED_EDGE('',*,*,#16972,.T.);
#22154=ORIENTED_EDGE('',*,*,#16970,.T.);
#22155=ORIENTED_EDGE('',*,*,#16967,.T.);
#22156=ORIENTED_EDGE('',*,*,#16976,.T.);
#22157=ORIENTED_EDGE('',*,*,#16980,.F.);
#31151=PLANE('',#34401);
#31152=PLANE('',#34405);
#31153=PLANE('',#34411);
#31154=PLANE('',#34413);
#31155=PLANE('',#34414);
#31156=PLANE('',#34415);
#31157=PLANE('',#34416);
#31158=PLANE('',#34417);
#31159=PLANE('',#34418);
#32053=ADVANCED_FACE('',(#4372),#888,.F.);
#32054=ADVANCED_FACE('',(#4373),#1093,.T.);
#32055=ADVANCED_FACE('',(#4374,#1897),#31151,.T.);
#32056=ADVANCED_FACE('',(#4375),#565,.T.);
#32057=ADVANCED_FACE('',(#4376),#31152,.T.);
#32058=ADVANCED_FACE('',(#4377),#889,.T.);
#32059=ADVANCED_FACE('',(#4378,#1898),#31153,.T.);
#32060=ADVANCED_FACE('',(#4379),#1094,.T.);
#32061=ADVANCED_FACE('',(#4380),#31154,.F.);
#32062=ADVANCED_FACE('',(#4381),#31155,.F.);
#32063=ADVANCED_FACE('',(#4382),#31156,.F.);
#32064=ADVANCED_FACE('',(#4383),#31157,.F.);
#32065=ADVANCED_FACE('',(#4384),#31158,.F.);
#32066=ADVANCED_FACE('',(#4385),#31159,.F.);
#32067=ADVANCED_FACE('',(#4386),#566,.F.);
#33793=CLOSED_SHELL('',(#32053,#32054,#32055,#32056,#32057,#32058,#32059,
#32060,#32061,#32062,#32063,#32064,#32065,#32066,#32067));
#34392=AXIS2_PLACEMENT_3D('',#50960,#38857,#38858);
#34393=AXIS2_PLACEMENT_3D('',#50961,#38859,#38860);
#34394=AXIS2_PLACEMENT_3D('',#50964,#38861,#38862);
#34395=AXIS2_PLACEMENT_3D('',#50965,#38863,#38864);
#34396=AXIS2_PLACEMENT_3D('',#50967,#38865,#38866);
#34397=AXIS2_PLACEMENT_3D('',#50968,#38867,#38868);
#34398=AXIS2_PLACEMENT_3D('',#50969,#38869,#38870);
#34399=AXIS2_PLACEMENT_3D('',#50972,#38871,#38872);
#34400=AXIS2_PLACEMENT_3D('',#50973,#38873,#38874);
#34401=AXIS2_PLACEMENT_3D('',#50975,#38876,#38877);
#34402=AXIS2_PLACEMENT_3D('',#50977,#38878,#38879);
#34403=AXIS2_PLACEMENT_3D('',#50978,#38880,#38881);
#34404=AXIS2_PLACEMENT_3D('',#50981,#38883,#38884);
#34405=AXIS2_PLACEMENT_3D('',#50982,#38885,#38886);
#34406=AXIS2_PLACEMENT_3D('',#50983,#38887,#38888);
#34407=AXIS2_PLACEMENT_3D('',#50986,#38889,#38890);
#34408=AXIS2_PLACEMENT_3D('',#50987,#38891,#38892);
#34409=AXIS2_PLACEMENT_3D('',#50989,#38893,#38894);
#34410=AXIS2_PLACEMENT_3D('',#50990,#38895,#38896);
#34411=AXIS2_PLACEMENT_3D('',#50991,#38897,#38898);
#34412=AXIS2_PLACEMENT_3D('',#51004,#38905,#38906);
#34413=AXIS2_PLACEMENT_3D('',#51006,#38908,#38909);
#34414=AXIS2_PLACEMENT_3D('',#51014,#38912,#38913);
#34415=AXIS2_PLACEMENT_3D('',#51020,#38915,#38916);
#34416=AXIS2_PLACEMENT_3D('',#51026,#38918,#38919);
#34417=AXIS2_PLACEMENT_3D('',#51032,#38921,#38922);
#34418=AXIS2_PLACEMENT_3D('',#51042,#38924,#38925);
#34419=AXIS2_PLACEMENT_3D('',#51046,#38926,#38927);
#38857=DIRECTION('axis',(0.,0.,1.));
#38858=DIRECTION('refdir',(1.,0.,0.));
#38859=DIRECTION('center_axis',(-5.00596043934461E-16,-1.,-1.12083973155589E-15));
#38860=DIRECTION('ref_axis',(1.,0.,-9.16829336464647E-15));
#38861=DIRECTION('center_axis',(5.00596043934461E-16,1.,1.12083973155589E-15));
#38862=DIRECTION('ref_axis',(-5.58323629842488E-15,1.12083973155589E-15,
-1.));
#38863=DIRECTION('center_axis',(5.00596043934461E-16,1.,1.12083973155589E-15));
#38864=DIRECTION('ref_axis',(-5.58323629842488E-15,1.12083973155589E-15,
-1.));
#38865=DIRECTION('center_axis',(0.,-1.12083973155589E-15,1.));
#38866=DIRECTION('ref_axis',(-1.,0.,0.));
#38867=DIRECTION('center_axis',(-5.00596043934461E-16,-1.,-1.12083973155589E-15));
#38868=DIRECTION('ref_axis',(-5.58323629842488E-15,1.12083973155589E-15,
-1.));
#38869=DIRECTION('center_axis',(-5.00596043934461E-16,-1.,-1.12083973155589E-15));
#38870=DIRECTION('ref_axis',(5.46077161851015E-15,-1.12083973155589E-15,
1.));
#38871=DIRECTION('center_axis',(-5.00596043934461E-16,-1.,-1.12083973155589E-15));
#38872=DIRECTION('ref_axis',(-5.46077161851015E-15,1.12083973155589E-15,
-1.));
#38873=DIRECTION('center_axis',(-5.00596043934461E-16,-1.,-1.12083973155589E-15));
#38874=DIRECTION('ref_axis',(-5.46077161851015E-15,1.12083973155589E-15,
-1.));
#38875=DIRECTION('',(5.00596043934461E-16,1.,1.12083973155589E-15));
#38876=DIRECTION('center_axis',(-5.00596043934461E-16,-1.,-1.12083973155589E-15));
#38877=DIRECTION('ref_axis',(1.,-5.00596043934455E-16,-5.46077161851015E-15));
#38878=DIRECTION('center_axis',(-5.00596043934461E-16,-1.,-1.12083973155589E-15));
#38879=DIRECTION('ref_axis',(5.46077161851015E-15,-1.12083973155589E-15,
1.));
#38880=DIRECTION('center_axis',(5.00596043934461E-16,1.,1.12083973155589E-15));
#38881=DIRECTION('ref_axis',(-5.46077161851015E-15,1.12083973155589E-15,
-1.));
#38882=DIRECTION('',(-4.30191910488433E-15,-0.707106781186548,-0.707106781186547));
#38883=DIRECTION('center_axis',(5.00596043934461E-16,1.,1.12083973155589E-15));
#38884=DIRECTION('ref_axis',(-5.46077161851015E-15,1.12083973155589E-15,
-1.));
#38885=DIRECTION('center_axis',(-5.00596043934461E-16,-1.,-1.12083973155589E-15));
#38886=DIRECTION('ref_axis',(1.,-5.00596043934455E-16,-5.46077161851015E-15));
#38887=DIRECTION('center_axis',(-5.00596043934461E-16,-1.,-1.12083973155589E-15));
#38888=DIRECTION('ref_axis',(1.,-7.89491928622333E-16,-6.31593542897867E-15));
#38889=DIRECTION('center_axis',(5.00596043934461E-16,1.,1.12083973155589E-15));
#38890=DIRECTION('ref_axis',(-5.58323629842488E-15,1.12083973155589E-15,
-1.));
#38891=DIRECTION('center_axis',(5.00596043934461E-16,1.,1.12083973155589E-15));
#38892=DIRECTION('ref_axis',(-5.58323629842488E-15,1.12083973155589E-15,
-1.));
#38893=DIRECTION('center_axis',(-7.89491928622335E-15,1.1208397315559E-15,
-1.));
#38894=DIRECTION('ref_axis',(-1.,9.86864910777919E-16,7.89491928622335E-15));
#38895=DIRECTION('center_axis',(-5.00596043934461E-16,-1.,-1.12083973155589E-15));
#38896=DIRECTION('ref_axis',(-5.58323629842488E-15,1.12083973155589E-15,
-1.));
#38897=DIRECTION('center_axis',(5.00596043934461E-16,1.,1.12083973155589E-15));
#38898=DIRECTION('ref_axis',(-1.,5.00596043934455E-16,5.46077161851015E-15));
#38899=DIRECTION('',(-1.,5.00596043934454E-16,6.22995669306358E-15));
#38900=DIRECTION('',(-0.500000000000005,1.22097370306556E-15,-0.866025403784436));
#38901=DIRECTION('',(0.499999999999995,7.20377659131108E-16,-0.866025403784441));
#38902=DIRECTION('',(1.,-5.00596043934455E-16,-5.55691975282933E-15));
#38903=DIRECTION('',(0.500000000000005,-1.22097370306556E-15,0.866025403784436));
#38904=DIRECTION('',(-0.499999999999995,-7.20377659131108E-16,0.866025403784441));
#38905=DIRECTION('center_axis',(-5.00596043934461E-16,-1.,-1.12083973155589E-15));
#38906=DIRECTION('ref_axis',(5.46077161851015E-15,-1.12083973155589E-15,
1.));
#38907=DIRECTION('',(5.00596043934461E-16,1.,1.12083973155589E-15));
#38908=DIRECTION('center_axis',(0.866025403784436,1.26890974696718E-16,
-0.500000000000005));
#38909=DIRECTION('ref_axis',(5.00353318950476E-16,1.,1.12041931955136E-15));
#38910=DIRECTION('',(5.00596043934461E-16,1.,1.12083973155589E-15));
#38911=DIRECTION('',(5.00596043934461E-16,1.,1.12083973155589E-15));
#38912=DIRECTION('center_axis',(0.866025403784442,-9.93948756859176E-16,
0.499999999999995));
#38913=DIRECTION('ref_axis',(5.00838768918447E-16,1.,1.12041931955136E-15));
#38914=DIRECTION('',(5.00596043934461E-16,1.,1.12083973155589E-15));
#38915=DIRECTION('center_axis',(6.22995669306358E-15,-1.1208397315559E-15,
1.));
#38916=DIRECTION('ref_axis',(-1.,5.00596043934454E-16,6.22995669306358E-15));
#38917=DIRECTION('',(5.00596043934461E-16,1.,1.12083973155589E-15));
#38918=DIRECTION('center_axis',(-0.866025403784436,-1.26890974696719E-16,
0.500000000000005));
#38919=DIRECTION('ref_axis',(-5.00353318950476E-16,-1.,-1.12041931955136E-15));
#38920=DIRECTION('',(-5.00596043934461E-16,-1.,-1.12083973155589E-15));
#38921=DIRECTION('center_axis',(-5.55691975282933E-15,1.12083973155589E-15,
-1.));
#38922=DIRECTION('ref_axis',(1.,-5.00596043934455E-16,-5.55691975282933E-15));
#38923=DIRECTION('',(5.00596043934461E-16,1.,1.12083973155589E-15));
#38924=DIRECTION('center_axis',(-0.866025403784442,9.93948756859176E-16,
-0.499999999999995));
#38925=DIRECTION('ref_axis',(-5.00838768918447E-16,-1.,-1.12041931955136E-15));
#38926=DIRECTION('center_axis',(5.00596043934461E-16,1.,1.12083973155589E-15));
#38927=DIRECTION('ref_axis',(5.46077161851015E-15,-1.12083973155589E-15,
1.));
#38928=DIRECTION('',(-4.58492644780011E-15,0.500000000000001,-0.866025403784438));
#50960=CARTESIAN_POINT('',(0.,0.,0.));
#50961=CARTESIAN_POINT('Origin',(221.615917770968,-69.5720072687899,403.500000551893));
#50962=CARTESIAN_POINT('',(215.615917770968,-69.5720072687899,403.500000551893));
#50963=CARTESIAN_POINT('',(221.615917770968,-69.5720072687899,397.500000551893));
#50964=CARTESIAN_POINT('Origin',(221.615917770968,-69.5720072687899,403.500000551893));
#50965=CARTESIAN_POINT('Origin',(221.615917770968,-69.5720072687899,403.500000551893));
#50966=CARTESIAN_POINT('',(215.515917770968,-69.4720072687899,403.500000551893));
#50967=CARTESIAN_POINT('Origin',(215.515917770968,-69.5720072687899,403.500000551893));
#50968=CARTESIAN_POINT('Origin',(221.615917770968,-69.4720072687899,403.500000551893));
#50969=CARTESIAN_POINT('Origin',(221.615917770968,-86.6595072687899,403.500000551893));
#50970=CARTESIAN_POINT('',(221.615917770968,-98.39846976879,409.500000551893));
#50971=CARTESIAN_POINT('',(221.615917770968,-98.3984697687899,397.500000551893));
#50972=CARTESIAN_POINT('Origin',(221.615917770968,-98.3984697687899,403.500000551893));
#50973=CARTESIAN_POINT('Origin',(221.615917770968,-98.3984697687899,403.500000551893));
#50974=CARTESIAN_POINT('',(221.615917770968,-86.6595072687899,397.500000551893));
#50975=CARTESIAN_POINT('Origin',(221.615917770968,-69.4720072687899,411.000000551893));
#50976=CARTESIAN_POINT('',(221.615917770968,-69.4720072687899,394.500000551893));
#50977=CARTESIAN_POINT('Origin',(221.615917770968,-69.4720072687899,403.500000551893));
#50978=CARTESIAN_POINT('Origin',(221.615917770968,-98.9352385187899,403.500000551893));
#50979=CARTESIAN_POINT('',(221.615917770968,-99.4720072687899,408.426463051893));
#50980=CARTESIAN_POINT('',(221.615917770968,-98.9352385187899,408.963231801893));
#50981=CARTESIAN_POINT('Origin',(221.615917770968,-99.4720072687899,403.500000551893));
#50982=CARTESIAN_POINT('Origin',(221.615917770968,-99.4720072687899,406.500000551893));
#50983=CARTESIAN_POINT('Origin',(221.615917770968,-58.6720072687899,403.500000551893));
#50984=CARTESIAN_POINT('',(212.615917770968,-58.6720072687899,403.500000551893));
#50985=CARTESIAN_POINT('',(221.615917770968,-58.6720072687899,394.500000551893));
#50986=CARTESIAN_POINT('Origin',(221.615917770968,-58.6720072687899,403.500000551893));
#50987=CARTESIAN_POINT('Origin',(221.615917770968,-58.6720072687899,403.500000551893));
#50988=CARTESIAN_POINT('',(213.815917770968,-57.4720072687899,403.500000551893));
#50989=CARTESIAN_POINT('Origin',(213.815917770968,-58.6720072687899,403.500000551893));
#50990=CARTESIAN_POINT('Origin',(221.615917770968,-57.4720072687899,403.500000551893));
#50991=CARTESIAN_POINT('Origin',(221.615917770968,-57.4720072687899,410.886751897841));
#50992=CARTESIAN_POINT('',(224.502669116916,-57.4720072687899,408.500000551893));
#50993=CARTESIAN_POINT('',(218.72916642502,-57.4720072687899,408.500000551893));
#50994=CARTESIAN_POINT('',(220.172542097994,-57.4720072687899,408.500000551893));
#50995=CARTESIAN_POINT('',(215.842415079072,-57.4720072687899,403.500000551893));
#50996=CARTESIAN_POINT('',(216.564102915559,-57.4720072687899,404.750000551893));
#50997=CARTESIAN_POINT('',(218.72916642502,-57.4720072687899,398.500000551893));
#50998=CARTESIAN_POINT('',(218.007478588533,-57.4720072687899,399.750000551893));
#50999=CARTESIAN_POINT('',(224.502669116916,-57.4720072687899,398.500000551893));
#51000=CARTESIAN_POINT('',(223.059293443942,-57.4720072687899,398.500000551893));
#51001=CARTESIAN_POINT('',(227.389420462865,-57.4720072687899,403.500000551893));
#51002=CARTESIAN_POINT('',(226.667732626378,-57.4720072687899,402.250000551893));
#51003=CARTESIAN_POINT('',(225.224356953403,-57.4720072687899,407.250000551893));
#51004=CARTESIAN_POINT('Origin',(221.615917770968,-63.4720072687899,403.500000551893));
#51005=CARTESIAN_POINT('',(221.615917770968,-63.4720072687899,394.500000551893));
#51006=CARTESIAN_POINT('Origin',(227.389420462865,-57.4720072687899,403.500000551893));
#51007=CARTESIAN_POINT('',(227.389420462865,-63.4720072687899,403.500000551893));
#51008=CARTESIAN_POINT('',(224.502669116916,-63.4720072687899,398.500000551893));
#51009=CARTESIAN_POINT('Ctrl Pts',(227.389420462865,-63.4720072687899,403.500000551893));
#51010=CARTESIAN_POINT('Ctrl Pts',(225.94604478989,-64.3053406021233,401.000000551893));
#51011=CARTESIAN_POINT('Ctrl Pts',(224.502669116916,-63.4720072687899,398.500000551893));
#51012=CARTESIAN_POINT('',(227.389420462865,-60.4720072687899,403.500000551893));
#51013=CARTESIAN_POINT('',(224.502669116916,-60.4720072687899,398.500000551893));
#51014=CARTESIAN_POINT('Origin',(224.502669116916,-57.4720072687899,408.500000551893));
#51015=CARTESIAN_POINT('',(224.502669116916,-63.4720072687899,408.500000551893));
#51016=CARTESIAN_POINT('Ctrl Pts',(224.502669116916,-63.4720072687899,408.500000551893));
#51017=CARTESIAN_POINT('Ctrl Pts',(225.946044789891,-64.3053406021233,406.000000551893));
#51018=CARTESIAN_POINT('Ctrl Pts',(227.389420462865,-63.4720072687899,403.500000551893));
#51019=CARTESIAN_POINT('',(224.502669116916,-60.4720072687899,408.500000551893));
#51020=CARTESIAN_POINT('Origin',(218.72916642502,-57.4720072687899,408.500000551893));
#51021=CARTESIAN_POINT('',(218.72916642502,-63.4720072687899,408.500000551893));
#51022=CARTESIAN_POINT('Ctrl Pts',(218.72916642502,-63.4720072687899,408.500000551893));
#51023=CARTESIAN_POINT('Ctrl Pts',(221.615917770968,-64.3053406021233,408.500000551893));
#51024=CARTESIAN_POINT('Ctrl Pts',(224.502669116916,-63.4720072687899,408.500000551893));
#51025=CARTESIAN_POINT('',(218.72916642502,-60.4720072687899,408.500000551893));
#51026=CARTESIAN_POINT('Origin',(215.842415079072,-57.4720072687899,403.500000551893));
#51027=CARTESIAN_POINT('',(215.842415079072,-63.4720072687899,403.500000551893));
#51028=CARTESIAN_POINT('Ctrl Pts',(215.842415079072,-63.4720072687899,403.500000551893));
#51029=CARTESIAN_POINT('Ctrl Pts',(217.285790752046,-64.3053406021233,406.000000551893));
#51030=CARTESIAN_POINT('Ctrl Pts',(218.72916642502,-63.4720072687899,408.500000551893));
#51031=CARTESIAN_POINT('',(215.842415079072,-60.4720072687899,403.500000551893));
#51032=CARTESIAN_POINT('Origin',(224.502669116916,-57.4720072687899,398.500000551893));
#51033=CARTESIAN_POINT('',(221.615917770968,-63.9185892561751,398.500000551893));
#51034=CARTESIAN_POINT('Ctrl Pts',(224.502669116916,-63.4720072687899,398.500000551893));
#51035=CARTESIAN_POINT('Ctrl Pts',(222.955663733124,-63.9185892561751,398.500000551893));
#51036=CARTESIAN_POINT('Ctrl Pts',(221.615917770968,-63.9185892561751,398.500000551893));
#51037=CARTESIAN_POINT('',(218.72916642502,-63.4720072687899,398.500000551893));
#51038=CARTESIAN_POINT('',(218.72916642502,-60.4720072687899,398.500000551893));
#51039=CARTESIAN_POINT('Ctrl Pts',(221.615917770968,-63.9185892561751,398.500000551893));
#51040=CARTESIAN_POINT('Ctrl Pts',(220.276171808813,-63.9185892561751,398.500000551893));
#51041=CARTESIAN_POINT('Ctrl Pts',(218.72916642502,-63.4720072687899,398.500000551893));
#51042=CARTESIAN_POINT('Origin',(218.72916642502,-57.4720072687899,398.500000551893));
#51043=CARTESIAN_POINT('Ctrl Pts',(218.72916642502,-63.4720072687899,398.500000551893));
#51044=CARTESIAN_POINT('Ctrl Pts',(217.285790752046,-64.3053406021233,401.000000551893));
#51045=CARTESIAN_POINT('Ctrl Pts',(215.842415079072,-63.4720072687899,403.500000551893));
#51046=CARTESIAN_POINT('Origin',(221.615917770968,-65.1386739354566,403.500000551893));
#51047=CARTESIAN_POINT('',(221.615917770968,-66.8053406021233,403.500000551893));
#51048=CARTESIAN_POINT('',(221.615917770968,-65.1386739354566,400.613249205945));
#61753=UNCERTAINTY_MEASURE_WITH_UNIT(LENGTH_MEASURE(0.01),#61812,
'DISTANCE_ACCURACY_VALUE',
'Maximum model space distance between geometric entities at asserted c
onnectivities');
#61780=UNCERTAINTY_MEASURE_WITH_UNIT(LENGTH_MEASURE(0.01),#61812,
'DISTANCE_ACCURACY_VALUE',
'Maximum model space distance between geometric entities at asserted c
onnectivities');
#61784=(
GEOMETRIC_REPRESENTATION_CONTEXT(3)
GLOBAL_UNCERTAINTY_ASSIGNED_CONTEXT((#61753))
GLOBAL_UNIT_ASSIGNED_CONTEXT((#61812,#61814,#61815))
REPRESENTATION_CONTEXT('','3D')
);
#61811=(
GEOMETRIC_REPRESENTATION_CONTEXT(3)
GLOBAL_UNCERTAINTY_ASSIGNED_CONTEXT((#61780))
GLOBAL_UNIT_ASSIGNED_CONTEXT((#61812,#61814,#61815))
REPRESENTATION_CONTEXT('','3D')
);
#61812=(
LENGTH_UNIT()
NAMED_UNIT(*)
SI_UNIT(.MILLI.,.METRE.)
);
#61814=(
NAMED_UNIT(*)
PLANE_ANGLE_UNIT()
SI_UNIT($,.RADIAN.)
);
#61815=(
NAMED_UNIT(*)
SI_UNIT($,.STERADIAN.)
SOLID_ANGLE_UNIT()
);
#61819=SHAPE_DEFINITION_REPRESENTATION(#61849,#61971);
#61849=PRODUCT_DEFINITION_SHAPE('',$,#62002);
#61971=SHAPE_REPRESENTATION('',(#34392),#61784);
#61998=PRODUCT_DEFINITION_CONTEXT('part definition',#62090,'design');
#62002=PRODUCT_DEFINITION('Bearing Housing Socket Screws',
'Bearing Housing Socket Screws',#62032,#61998);
#62032=PRODUCT_DEFINITION_FORMATION('',$,#62095);
#62090=APPLICATION_CONTEXT('Managed model based 3d engineering');
#62091=PRODUCT_CONTEXT('part definition',#62090,'mechanical');
#62095=PRODUCT('Bearing Housing Socket Screws',
'Bearing Housing Socket Screws',$,(#62091));
#62157=COLOUR_RGB('Black',0.12,0.14,0.17);
#62158=FILL_AREA_STYLE_COLOUR('',#62157);
#62159=FILL_AREA_STYLE('',(#62158));
#62160=SURFACE_STYLE_FILL_AREA(#62159);
#62161=SURFACE_SIDE_STYLE('',(#62160));
#62162=SURFACE_STYLE_USAGE(.BOTH.,#62161);
#62163=PRESENTATION_STYLE_ASSIGNMENT((#62162));
ENDSEC;
END-ISO-10303-21;
